ISO-10303-21;
HEADER;
/* Generated by software containing ST-Developer
 * from STEP Tools, Inc. (www.steptools.com) 
 */

FILE_DESCRIPTION(
/* description */ ('Two-link friction support arm'),
/* implementation_level */ '2;1');

FILE_NAME(
/* name */ 'Hex Bolt - M8x40.step',
/* time_stamp */ '2026-10-27T20:01:49-07:00',
/* author */ (''),
/* organization */ (''),
/* preprocessor_version */ 'ST-DEVELOPER v20.2',
/* originating_system */ 'Autodesk Translation Framework v15.17.0.0',
/* authorisation */ '');

FILE_SCHEMA (('AUTOMOTIVE_DESIGN { 1 0 10303 214 3 1 1 }'));
ENDSEC;

DATA;
#10=MECHANICAL_DESIGN_GEOMETRIC_PRESENTATION_REPRESENTATION('',(#201),#5492);
#143=(
BOUNDED_CURVE()
B_SPLINE_CURVE(2,(#5086,#5087,#5088),.UNSPECIFIED.,.F.,.F.)
B_SPLINE_CURVE_WITH_KNOTS((3,3),(0.14973948338295,0.97160236658079),
 .UNSPECIFIED.)
CURVE()
GEOMETRIC_REPRESENTATION_ITEM()
RATIONAL_B_SPLINE_CURVE((1.07140024848292,1.23714644374248,1.07140024848292))
REPRESENTATION_ITEM('')
);
#144=(
BOUNDED_CURVE()
B_SPLINE_CURVE(2,(#5090,#5091,#5092),.UNSPECIFIED.,.F.,.F.)
B_SPLINE_CURVE_WITH_KNOTS((3,3),(0.14973948338295,0.97160236658079),
 .UNSPECIFIED.)
CURVE()
GEOMETRIC_REPRESENTATION_ITEM()
RATIONAL_B_SPLINE_CURVE((1.07140024848292,1.23714644374248,1.07140024848292))
REPRESENTATION_ITEM('')
);
#145=(
BOUNDED_CURVE()
B_SPLINE_CURVE(2,(#5094,#5095,#5096),.UNSPECIFIED.,.F.,.F.)
B_SPLINE_CURVE_WITH_KNOTS((3,3),(0.14973948338295,0.97160236658079),
 .UNSPECIFIED.)
CURVE()
GEOMETRIC_REPRESENTATION_ITEM()
RATIONAL_B_SPLINE_CURVE((1.07140024848292,1.23714644374248,1.07140024848292))
REPRESENTATION_ITEM('')
);
#146=(
BOUNDED_CURVE()
B_SPLINE_CURVE(2,(#5098,#5099,#5100),.UNSPECIFIED.,.F.,.F.)
B_SPLINE_CURVE_WITH_KNOTS((3,3),(0.149739483382949,0.971602366580789),
 .UNSPECIFIED.)
CURVE()
GEOMETRIC_REPRESENTATION_ITEM()
RATIONAL_B_SPLINE_CURVE((1.07140024848292,1.23714644374248,1.07140024848292))
REPRESENTATION_ITEM('')
);
#147=(
BOUNDED_CURVE()
B_SPLINE_CURVE(2,(#5102,#5103,#5104),.UNSPECIFIED.,.F.,.F.)
B_SPLINE_CURVE_WITH_KNOTS((3,3),(0.14973948338295,0.971602366580789),
 .UNSPECIFIED.)
CURVE()
GEOMETRIC_REPRESENTATION_ITEM()
RATIONAL_B_SPLINE_CURVE((1.07140024848292,1.23714644374248,1.07140024848292))
REPRESENTATION_ITEM('')
);
#148=(
BOUNDED_CURVE()
B_SPLINE_CURVE(2,(#5105,#5106,#5107),.UNSPECIFIED.,.F.,.F.)
B_SPLINE_CURVE_WITH_KNOTS((3,3),(0.14973948338295,0.97160236658079),
 .UNSPECIFIED.)
CURVE()
GEOMETRIC_REPRESENTATION_ITEM()
RATIONAL_B_SPLINE_CURVE((1.07140024848292,1.23714644374248,1.07140024848292))
REPRESENTATION_ITEM('')
);
#167=CONICAL_SURFACE('',#3456,0.36,0.785398163397451);
#168=CONICAL_SURFACE('',#3459,0.734027674973257,1.0471975511966);
#179=SHAPE_REPRESENTATION_RELATIONSHIP('SRR','None',#5572,#190);
#190=ADVANCED_BREP_SHAPE_REPRESENTATION('',(#211),#5486);
#201=STYLED_ITEM('',(#5708),#211);
#211=MANIFOLD_SOLID_BREP('Body1',#3178);
#232=FACE_BOUND('',#671,.T.);
#336=PLANE('',#3458);
#337=PLANE('',#3461);
#338=PLANE('',#3462);
#339=PLANE('',#3463);
#340=PLANE('',#3464);
#341=PLANE('',#3465);
#342=PLANE('',#3466);
#343=PLANE('',#3467);
#344=PLANE('',#3468);
#476=FACE_OUTER_BOUND('',#659,.T.);
#477=FACE_OUTER_BOUND('',#660,.T.);
#478=FACE_OUTER_BOUND('',#661,.T.);
#479=FACE_OUTER_BOUND('',#662,.T.);
#480=FACE_OUTER_BOUND('',#663,.T.);
#481=FACE_OUTER_BOUND('',#664,.T.);
#482=FACE_OUTER_BOUND('',#665,.T.);
#483=FACE_OUTER_BOUND('',#666,.T.);
#484=FACE_OUTER_BOUND('',#667,.T.);
#485=FACE_OUTER_BOUND('',#668,.T.);
#486=FACE_OUTER_BOUND('',#669,.T.);
#487=FACE_OUTER_BOUND('',#670,.T.);
#659=EDGE_LOOP('',(#2664,#2665,#2666,#2667));
#660=EDGE_LOOP('',(#2668,#2669,#2670,#2671));
#661=EDGE_LOOP('',(#2672));
#662=EDGE_LOOP('',(#2673,#2674,#2675,#2676,#2677,#2678,#2679,#2680,#2681));
#663=EDGE_LOOP('',(#2682,#2683,#2684,#2685));
#664=EDGE_LOOP('',(#2686,#2687,#2688,#2689));
#665=EDGE_LOOP('',(#2690,#2691,#2692,#2693));
#666=EDGE_LOOP('',(#2694,#2695,#2696,#2697));
#667=EDGE_LOOP('',(#2698,#2699,#2700,#2701));
#668=EDGE_LOOP('',(#2702,#2703,#2704,#2705));
#669=EDGE_LOOP('',(#2706));
#670=EDGE_LOOP('',(#2707,#2708,#2709,#2710,#2711,#2712));
#671=EDGE_LOOP('',(#2713));
#970=LINE('',#5073,#1283);
#971=LINE('',#5078,#1284);
#972=LINE('',#5084,#1285);
#973=LINE('',#5110,#1286);
#974=LINE('',#5112,#1287);
#975=LINE('',#5113,#1288);
#976=LINE('',#5116,#1289);
#977=LINE('',#5117,#1290);
#978=LINE('',#5120,#1291);
#979=LINE('',#5121,#1292);
#980=LINE('',#5124,#1293);
#981=LINE('',#5125,#1294);
#982=LINE('',#5128,#1295);
#983=LINE('',#5129,#1296);
#984=LINE('',#5131,#1297);
#1283=VECTOR('',#4134,0.4);
#1284=VECTOR('',#4141,0.36);
#1285=VECTOR('',#4148,0.734027674973257);
#1286=VECTOR('',#4151,1.);
#1287=VECTOR('',#4152,1.);
#1288=VECTOR('',#4153,1.);
#1289=VECTOR('',#4156,1.);
#1290=VECTOR('',#4157,1.);
#1291=VECTOR('',#4160,1.);
#1292=VECTOR('',#4161,1.);
#1293=VECTOR('',#4164,1.);
#1294=VECTOR('',#4165,1.);
#1295=VECTOR('',#4168,1.);
#1296=VECTOR('',#4169,1.);
#1297=VECTOR('',#4172,1.);
#1399=CIRCLE('',#3454,0.3933);
#1400=CIRCLE('',#3455,0.3933);
#1401=CIRCLE('',#3457,0.32);
#1402=CIRCLE('',#3460,0.6175);
#1623=VERTEX_POINT('',#5070);
#1624=VERTEX_POINT('',#5072);
#1625=VERTEX_POINT('',#5076);
#1626=VERTEX_POINT('',#5081);
#1627=VERTEX_POINT('',#5083);
#1628=VERTEX_POINT('',#5085);
#1629=VERTEX_POINT('',#5089);
#1630=VERTEX_POINT('',#5093);
#1631=VERTEX_POINT('',#5097);
#1632=VERTEX_POINT('',#5101);
#1633=VERTEX_POINT('',#5109);
#1634=VERTEX_POINT('',#5111);
#1635=VERTEX_POINT('',#5115);
#1636=VERTEX_POINT('',#5119);
#1637=VERTEX_POINT('',#5123);
#1638=VERTEX_POINT('',#5127);
#1986=EDGE_CURVE('',#1623,#1623,#1399,.F.);
#1987=EDGE_CURVE('',#1623,#1624,#970,.T.);
#1988=EDGE_CURVE('',#1624,#1624,#1400,.F.);
#1989=EDGE_CURVE('',#1625,#1625,#1401,.T.);
#1990=EDGE_CURVE('',#1625,#1623,#971,.T.);
#1991=EDGE_CURVE('',#1626,#1626,#1402,.T.);
#1992=EDGE_CURVE('',#1626,#1627,#972,.T.);
#1993=EDGE_CURVE('',#1628,#1627,#143,.T.);
#1994=EDGE_CURVE('',#1629,#1628,#144,.T.);
#1995=EDGE_CURVE('',#1630,#1629,#145,.T.);
#1996=EDGE_CURVE('',#1631,#1630,#146,.T.);
#1997=EDGE_CURVE('',#1632,#1631,#147,.T.);
#1998=EDGE_CURVE('',#1627,#1632,#148,.T.);
#1999=EDGE_CURVE('',#1633,#1631,#973,.T.);
#2000=EDGE_CURVE('',#1633,#1634,#974,.T.);
#2001=EDGE_CURVE('',#1634,#1632,#975,.T.);
#2002=EDGE_CURVE('',#1635,#1630,#976,.T.);
#2003=EDGE_CURVE('',#1635,#1633,#977,.T.);
#2004=EDGE_CURVE('',#1636,#1629,#978,.T.);
#2005=EDGE_CURVE('',#1636,#1635,#979,.T.);
#2006=EDGE_CURVE('',#1637,#1628,#980,.T.);
#2007=EDGE_CURVE('',#1637,#1636,#981,.T.);
#2008=EDGE_CURVE('',#1638,#1627,#982,.T.);
#2009=EDGE_CURVE('',#1638,#1637,#983,.T.);
#2010=EDGE_CURVE('',#1634,#1638,#984,.T.);
#2664=ORIENTED_EDGE('',*,*,#1986,.F.);
#2665=ORIENTED_EDGE('',*,*,#1987,.T.);
#2666=ORIENTED_EDGE('',*,*,#1988,.F.);
#2667=ORIENTED_EDGE('',*,*,#1987,.F.);
#2668=ORIENTED_EDGE('',*,*,#1989,.F.);
#2669=ORIENTED_EDGE('',*,*,#1990,.T.);
#2670=ORIENTED_EDGE('',*,*,#1986,.T.);
#2671=ORIENTED_EDGE('',*,*,#1990,.F.);
#2672=ORIENTED_EDGE('',*,*,#1989,.T.);
#2673=ORIENTED_EDGE('',*,*,#1991,.F.);
#2674=ORIENTED_EDGE('',*,*,#1992,.T.);
#2675=ORIENTED_EDGE('',*,*,#1993,.F.);
#2676=ORIENTED_EDGE('',*,*,#1994,.F.);
#2677=ORIENTED_EDGE('',*,*,#1995,.F.);
#2678=ORIENTED_EDGE('',*,*,#1996,.F.);
#2679=ORIENTED_EDGE('',*,*,#1997,.F.);
#2680=ORIENTED_EDGE('',*,*,#1998,.F.);
#2681=ORIENTED_EDGE('',*,*,#1992,.F.);
#2682=ORIENTED_EDGE('',*,*,#1997,.T.);
#2683=ORIENTED_EDGE('',*,*,#1999,.F.);
#2684=ORIENTED_EDGE('',*,*,#2000,.T.);
#2685=ORIENTED_EDGE('',*,*,#2001,.T.);
#2686=ORIENTED_EDGE('',*,*,#1996,.T.);
#2687=ORIENTED_EDGE('',*,*,#2002,.F.);
#2688=ORIENTED_EDGE('',*,*,#2003,.T.);
#2689=ORIENTED_EDGE('',*,*,#1999,.T.);
#2690=ORIENTED_EDGE('',*,*,#1995,.T.);
#2691=ORIENTED_EDGE('',*,*,#2004,.F.);
#2692=ORIENTED_EDGE('',*,*,#2005,.T.);
#2693=ORIENTED_EDGE('',*,*,#2002,.T.);
#2694=ORIENTED_EDGE('',*,*,#1994,.T.);
#2695=ORIENTED_EDGE('',*,*,#2006,.F.);
#2696=ORIENTED_EDGE('',*,*,#2007,.T.);
#2697=ORIENTED_EDGE('',*,*,#2004,.T.);
#2698=ORIENTED_EDGE('',*,*,#1993,.T.);
#2699=ORIENTED_EDGE('',*,*,#2008,.F.);
#2700=ORIENTED_EDGE('',*,*,#2009,.T.);
#2701=ORIENTED_EDGE('',*,*,#2006,.T.);
#2702=ORIENTED_EDGE('',*,*,#1998,.T.);
#2703=ORIENTED_EDGE('',*,*,#2001,.F.);
#2704=ORIENTED_EDGE('',*,*,#2010,.T.);
#2705=ORIENTED_EDGE('',*,*,#2008,.T.);
#2706=ORIENTED_EDGE('',*,*,#1991,.T.);
#2707=ORIENTED_EDGE('',*,*,#2005,.F.);
#2708=ORIENTED_EDGE('',*,*,#2007,.F.);
#2709=ORIENTED_EDGE('',*,*,#2009,.F.);
#2710=ORIENTED_EDGE('',*,*,#2010,.F.);
#2711=ORIENTED_EDGE('',*,*,#2000,.F.);
#2712=ORIENTED_EDGE('',*,*,#2003,.F.);
#2713=ORIENTED_EDGE('',*,*,#1988,.T.);
#2981=CYLINDRICAL_SURFACE('',#3453,0.3933);
#3107=ADVANCED_FACE('',(#476),#2981,.T.);
#3108=ADVANCED_FACE('',(#477),#167,.T.);
#3109=ADVANCED_FACE('',(#478),#336,.T.);
#3110=ADVANCED_FACE('',(#479),#168,.T.);
#3111=ADVANCED_FACE('',(#480),#337,.T.);
#3112=ADVANCED_FACE('',(#481),#338,.T.);
#3113=ADVANCED_FACE('',(#482),#339,.T.);
#3114=ADVANCED_FACE('',(#483),#340,.T.);
#3115=ADVANCED_FACE('',(#484),#341,.T.);
#3116=ADVANCED_FACE('',(#485),#342,.T.);
#3117=ADVANCED_FACE('',(#486),#343,.T.);
#3118=ADVANCED_FACE('',(#487,#232),#344,.F.);
#3178=CLOSED_SHELL('',(#3107,#3108,#3109,#3110,#3111,#3112,#3113,#3114,
#3115,#3116,#3117,#3118));
#3452=AXIS2_PLACEMENT_3D('',#5068,#4128,#4129);
#3453=AXIS2_PLACEMENT_3D('',#5069,#4130,#4131);
#3454=AXIS2_PLACEMENT_3D('',#5071,#4132,#4133);
#3455=AXIS2_PLACEMENT_3D('',#5074,#4135,#4136);
#3456=AXIS2_PLACEMENT_3D('',#5075,#4137,#4138);
#3457=AXIS2_PLACEMENT_3D('',#5077,#4139,#4140);
#3458=AXIS2_PLACEMENT_3D('',#5079,#4142,#4143);
#3459=AXIS2_PLACEMENT_3D('',#5080,#4144,#4145);
#3460=AXIS2_PLACEMENT_3D('',#5082,#4146,#4147);
#3461=AXIS2_PLACEMENT_3D('',#5108,#4149,#4150);
#3462=AXIS2_PLACEMENT_3D('',#5114,#4154,#4155);
#3463=AXIS2_PLACEMENT_3D('',#5118,#4158,#4159);
#3464=AXIS2_PLACEMENT_3D('',#5122,#4162,#4163);
#3465=AXIS2_PLACEMENT_3D('',#5126,#4166,#4167);
#3466=AXIS2_PLACEMENT_3D('',#5130,#4170,#4171);
#3467=AXIS2_PLACEMENT_3D('',#5132,#4173,#4174);
#3468=AXIS2_PLACEMENT_3D('',#5133,#4175,#4176);
#4128=DIRECTION('axis',(0.,0.,1.));
#4129=DIRECTION('refdir',(1.,0.,0.));
#4130=DIRECTION('center_axis',(0.,-1.,0.));
#4131=DIRECTION('ref_axis',(1.,0.,0.));
#4132=DIRECTION('center_axis',(0.,1.,0.));
#4133=DIRECTION('ref_axis',(1.,0.,0.));
#4134=DIRECTION('',(0.,1.,0.));
#4135=DIRECTION('center_axis',(0.,-1.,0.));
#4136=DIRECTION('ref_axis',(1.,0.,0.));
#4137=DIRECTION('center_axis',(0.,1.,0.));
#4138=DIRECTION('ref_axis',(1.,0.,0.));
#4139=DIRECTION('center_axis',(0.,-1.,0.));
#4140=DIRECTION('ref_axis',(1.,0.,0.));
#4141=DIRECTION('',(-0.707106781186549,0.707106781186546,-8.65956056235496E-17));
#4142=DIRECTION('center_axis',(0.,-1.,0.));
#4143=DIRECTION('ref_axis',(0.,0.,-1.));
#4144=DIRECTION('center_axis',(0.,-1.,0.));
#4145=DIRECTION('ref_axis',(1.,0.,0.));
#4146=DIRECTION('center_axis',(0.,1.,0.));
#4147=DIRECTION('ref_axis',(1.,0.,0.));
#4148=DIRECTION('',(-0.866025403784439,-0.5,-1.06057523872491E-16));
#4149=DIRECTION('center_axis',(1.4792020664489E-16,0.,-1.));
#4150=DIRECTION('ref_axis',(-1.,0.,-1.4792020664489E-16));
#4151=DIRECTION('',(0.,1.,0.));
#4152=DIRECTION('',(-1.,0.,-1.4792020664489E-16));
#4153=DIRECTION('',(0.,1.,0.));
#4154=DIRECTION('center_axis',(0.866025403784439,0.,-0.5));
#4155=DIRECTION('ref_axis',(-0.5,0.,-0.866025403784439));
#4156=DIRECTION('',(0.,1.,0.));
#4157=DIRECTION('',(-0.5,0.,-0.866025403784439));
#4158=DIRECTION('center_axis',(0.866025403784439,0.,0.5));
#4159=DIRECTION('ref_axis',(0.5,0.,-0.866025403784439));
#4160=DIRECTION('',(0.,1.,0.));
#4161=DIRECTION('',(0.5,0.,-0.866025403784439));
#4162=DIRECTION('center_axis',(-2.95840413289779E-16,0.,1.));
#4163=DIRECTION('ref_axis',(1.,0.,2.95840413289779E-16));
#4164=DIRECTION('',(0.,1.,0.));
#4165=DIRECTION('',(1.,0.,2.95840413289779E-16));
#4166=DIRECTION('center_axis',(-0.866025403784439,0.,0.5));
#4167=DIRECTION('ref_axis',(0.5,0.,0.866025403784439));
#4168=DIRECTION('',(0.,1.,0.));
#4169=DIRECTION('',(0.5,0.,0.866025403784439));
#4170=DIRECTION('center_axis',(-0.866025403784439,0.,-0.5));
#4171=DIRECTION('ref_axis',(-0.5,0.,0.866025403784439));
#4172=DIRECTION('',(-0.5,0.,0.866025403784439));
#4173=DIRECTION('center_axis',(0.,1.,0.));
#4174=DIRECTION('ref_axis',(0.,0.,1.));
#4175=DIRECTION('center_axis',(0.,1.,0.));
#4176=DIRECTION('ref_axis',(1.,0.,0.));
#5068=CARTESIAN_POINT('',(0.,0.,0.));
#5069=CARTESIAN_POINT('Origin',(0.,-1.935,0.));
#5070=CARTESIAN_POINT('',(-0.3933,-3.9267,4.81653586104654E-17));
#5071=CARTESIAN_POINT('Origin',(0.,-3.9267,0.));
#5072=CARTESIAN_POINT('',(-0.3933,0.,-4.81653586104654E-17));
#5073=CARTESIAN_POINT('',(-0.3933,-1.935,-4.81653586104654E-17));
#5074=CARTESIAN_POINT('Origin',(0.,0.,0.));
#5075=CARTESIAN_POINT('Origin',(0.,-3.96,0.));
#5076=CARTESIAN_POINT('',(-0.32,-4.,-3.91886975727153E-17));
#5077=CARTESIAN_POINT('Origin',(0.,-4.,0.));
#5078=CARTESIAN_POINT('',(-0.36,-3.96,-4.40872847693047E-17));
#5079=CARTESIAN_POINT('Origin',(0.,-4.,0.));
#5080=CARTESIAN_POINT('Origin',(0.,0.462722715486149,0.));
#5081=CARTESIAN_POINT('',(-0.6175,0.53,-7.5621939847349E-17));
#5082=CARTESIAN_POINT('Origin',(0.,0.53,0.));
#5083=CARTESIAN_POINT('',(-0.750555349946514,0.453180457891261,-9.19165206894919E-17));
#5084=CARTESIAN_POINT('',(-0.734027674973257,0.462722715486149,-8.98924642641573E-17));
#5085=CARTESIAN_POINT('',(-0.375277674973257,0.453180457891261,0.65));
#5086=CARTESIAN_POINT('Ctrl Pts',(-0.375277674973257,0.45318045789126,0.65));
#5087=CARTESIAN_POINT('Ctrl Pts',(-0.562916512459968,0.561513791224244,
0.324999999999856));
#5088=CARTESIAN_POINT('Ctrl Pts',(-0.750555349946514,0.45318045789126,-9.19165206894919E-17));
#5089=CARTESIAN_POINT('',(0.375277674973257,0.453180457891261,0.65));
#5090=CARTESIAN_POINT('Ctrl Pts',(0.375277674973257,0.453180457891261,0.65));
#5091=CARTESIAN_POINT('Ctrl Pts',(-1.66922031752392E-13,0.561513791224244,
0.65));
#5092=CARTESIAN_POINT('Ctrl Pts',(-0.375277674973257,0.45318045789126,0.65));
#5093=CARTESIAN_POINT('',(0.750555349946514,0.453180457891261,0.));
#5094=CARTESIAN_POINT('Ctrl Pts',(0.750555349946514,0.453180457891261,0.));
#5095=CARTESIAN_POINT('Ctrl Pts',(0.562916512459802,0.561513791224244,0.325000000000144));
#5096=CARTESIAN_POINT('Ctrl Pts',(0.375277674973257,0.45318045789126,0.65));
#5097=CARTESIAN_POINT('',(0.375277674973257,0.453180457891261,-0.65));
#5098=CARTESIAN_POINT('Ctrl Pts',(0.375277674973257,0.45318045789126,-0.65));
#5099=CARTESIAN_POINT('Ctrl Pts',(0.562916512459968,0.561513791224244,-0.324999999999855));
#5100=CARTESIAN_POINT('Ctrl Pts',(0.750555349946514,0.453180457891261,0.));
#5101=CARTESIAN_POINT('',(-0.375277674973257,0.45318045789126,-0.65));
#5102=CARTESIAN_POINT('Ctrl Pts',(-0.375277674973257,0.453180457891261,
-0.65));
#5103=CARTESIAN_POINT('Ctrl Pts',(1.66866520601161E-13,0.561513791224244,
-0.65));
#5104=CARTESIAN_POINT('Ctrl Pts',(0.375277674973257,0.45318045789126,-0.65));
#5105=CARTESIAN_POINT('Ctrl Pts',(-0.750555349946514,0.453180457891261,
-9.19165206894919E-17));
#5106=CARTESIAN_POINT('Ctrl Pts',(-0.562916512459802,0.561513791224244,
-0.325000000000144));
#5107=CARTESIAN_POINT('Ctrl Pts',(-0.375277674973257,0.45318045789126,-0.65));
#5108=CARTESIAN_POINT('Origin',(0.375277674973257,0.,-0.65));
#5109=CARTESIAN_POINT('',(0.375277674973257,0.,-0.65));
#5110=CARTESIAN_POINT('',(0.375277674973257,0.,-0.65));
#5111=CARTESIAN_POINT('',(-0.375277674973257,0.,-0.65));
#5112=CARTESIAN_POINT('',(0.375277674973257,0.,-0.65));
#5113=CARTESIAN_POINT('',(-0.375277674973257,0.,-0.65));
#5114=CARTESIAN_POINT('Origin',(0.750555349946514,0.,0.));
#5115=CARTESIAN_POINT('',(0.750555349946514,0.,0.));
#5116=CARTESIAN_POINT('',(0.750555349946514,0.,0.));
#5117=CARTESIAN_POINT('',(0.750555349946514,0.,0.));
#5118=CARTESIAN_POINT('Origin',(0.375277674973257,0.,0.65));
#5119=CARTESIAN_POINT('',(0.375277674973257,0.,0.65));
#5120=CARTESIAN_POINT('',(0.375277674973257,0.,0.65));
#5121=CARTESIAN_POINT('',(0.375277674973257,0.,0.65));
#5122=CARTESIAN_POINT('Origin',(-0.375277674973257,0.,0.65));
#5123=CARTESIAN_POINT('',(-0.375277674973257,0.,0.65));
#5124=CARTESIAN_POINT('',(-0.375277674973257,0.,0.65));
#5125=CARTESIAN_POINT('',(-0.375277674973257,0.,0.65));
#5126=CARTESIAN_POINT('Origin',(-0.750555349946514,0.,-9.19165206894919E-17));
#5127=CARTESIAN_POINT('',(-0.750555349946514,0.,-9.19165206894919E-17));
#5128=CARTESIAN_POINT('',(-0.750555349946514,0.,-9.19165206894919E-17));
#5129=CARTESIAN_POINT('',(-0.750555349946514,0.,-9.19165206894919E-17));
#5130=CARTESIAN_POINT('Origin',(-0.375277674973257,0.,-0.65));
#5131=CARTESIAN_POINT('',(-0.375277674973257,0.,-0.65));
#5132=CARTESIAN_POINT('Origin',(0.,0.53,-1.11022302462516E-16));
#5133=CARTESIAN_POINT('Origin',(0.,0.,-1.11022302462516E-16));
#5469=UNCERTAINTY_MEASURE_WITH_UNIT(LENGTH_MEASURE(0.001),#5493,
'DISTANCE_ACCURACY_VALUE',
'Maximum model space distance between geometric entities at asserted c
onnectivities');
#5475=UNCERTAINTY_MEASURE_WITH_UNIT(LENGTH_MEASURE(0.001),#5493,
'DISTANCE_ACCURACY_VALUE',
'Maximum model space distance between geometric entities at asserted c
onnectivities');
#5486=(
GEOMETRIC_REPRESENTATION_CONTEXT(3)
GLOBAL_UNCERTAINTY_ASSIGNED_CONTEXT((#5469))
GLOBAL_UNIT_ASSIGNED_CONTEXT((#5493,#5495,#5496))
REPRESENTATION_CONTEXT('','3D')
);
#5492=(
GEOMETRIC_REPRESENTATION_CONTEXT(3)
GLOBAL_UNCERTAINTY_ASSIGNED_CONTEXT((#5475))
GLOBAL_UNIT_ASSIGNED_CONTEXT((#5493,#5495,#5496))
REPRESENTATION_CONTEXT('','3D')
);
#5493=(
LENGTH_UNIT()
NAMED_UNIT(*)
SI_UNIT(.CENTI.,.METRE.)
);
#5495=(
NAMED_UNIT(*)
PLANE_ANGLE_UNIT()
SI_UNIT($,.RADIAN.)
);
#5496=(
NAMED_UNIT(*)
SI_UNIT($,.STERADIAN.)
SOLID_ANGLE_UNIT()
);
#5507=SHAPE_DEFINITION_REPRESENTATION(#5523,#5572);
#5523=PRODUCT_DEFINITION_SHAPE('',$,#5589);
#5572=SHAPE_REPRESENTATION('',(#3452),#5486);
#5578=PRODUCT_DEFINITION_CONTEXT('part definition',#5628,'design');
#5589=PRODUCT_DEFINITION('Hex Bolt - M8x40','Hex Bolt - M8x40',#5605,#5578);
#5605=PRODUCT_DEFINITION_FORMATION('',$,#5640);
#5628=APPLICATION_CONTEXT(
'Core Data for Automotive Mechanical Design Process');
#5629=PRODUCT_CONTEXT('part definition',#5628,'mechanical');
#5640=PRODUCT('Hex Bolt - M8x40','Hex Bolt - M8x40','Hex Bolt - M8x40',
(#5629));
#5702=COLOUR_RGB('Black',0.12,0.14,0.17);
#5703=FILL_AREA_STYLE_COLOUR('',#5702);
#5704=FILL_AREA_STYLE('',(#5703));
#5705=SURFACE_STYLE_FILL_AREA(#5704);
#5706=SURFACE_SIDE_STYLE('',(#5705));
#5707=SURFACE_STYLE_USAGE(.BOTH.,#5706);
#5708=PRESENTATION_STYLE_ASSIGNMENT((#5707));
ENDSEC;
END-ISO-10303-21;
